ISO-10303-21;
HEADER;
/* Generated by software containing ST-Developer
 * from STEP Tools, Inc. (www.steptools.com) 
 */

FILE_DESCRIPTION(
/* description */ ('Hand wheel with handle and shaft collar'),
/* implementation_level */ '2;1');

FILE_NAME(
/* name */ 'M4x10 handle screw.step',
/* time_stamp */ '2026-10-28T03:23:19-07:00',
/* author */ (''),
/* organization */ (''),
/* preprocessor_version */ 'ST-DEVELOPER v20.2',
/* originating_system */ 'Autodesk Translation Framework v15.17.0.0',
/* authorisation */ '');

FILE_SCHEMA (('AUTOMOTIVE_DESIGN { 1 0 10303 214 3 1 1 }'));
ENDSEC;

DATA;
#10=MECHANICAL_DESIGN_GEOMETRIC_PRESENTATION_REPRESENTATION('',(#425),#10510);
#314=CONICAL_SURFACE('',#6181,0.325,0.785398163397448);
#315=CONICAL_SURFACE('',#6185,0.335,0.785398163397448);
#316=CONICAL_SURFACE('',#6189,0.21,0.463647609000806);
#326=ORIENTED_CLOSED_SHELL('',*,#5325,.F.);
#329=BREP_WITH_VOIDS('Body1',#5326,(#326));
#354=SHAPE_REPRESENTATION_RELATIONSHIP('SRR','None',#10672,#386);
#386=ADVANCED_BREP_SHAPE_REPRESENTATION('',(#329),#10499);
#425=STYLED_ITEM('',(#10915),#329);
#582=FACE_BOUND('',#1417,.T.);
#719=PLANE('',#6169);
#720=PLANE('',#6170);
#721=PLANE('',#6171);
#722=PLANE('',#6172);
#723=PLANE('',#6173);
#724=PLANE('',#6174);
#725=PLANE('',#6175);
#726=PLANE('',#6176);
#727=PLANE('',#6177);
#728=PLANE('',#6179);
#729=PLANE('',#6187);
#988=FACE_OUTER_BOUND('',#1403,.T.);
#989=FACE_OUTER_BOUND('',#1404,.T.);
#990=FACE_OUTER_BOUND('',#1405,.T.);
#991=FACE_OUTER_BOUND('',#1406,.T.);
#992=FACE_OUTER_BOUND('',#1407,.T.);
#993=FACE_OUTER_BOUND('',#1408,.T.);
#994=FACE_OUTER_BOUND('',#1409,.T.);
#995=FACE_OUTER_BOUND('',#1410,.T.);
#996=FACE_OUTER_BOUND('',#1411,.T.);
#997=FACE_OUTER_BOUND('',#1412,.T.);
#998=FACE_OUTER_BOUND('',#1413,.T.);
#999=FACE_OUTER_BOUND('',#1414,.T.);
#1000=FACE_OUTER_BOUND('',#1415,.T.);
#1001=FACE_OUTER_BOUND('',#1416,.T.);
#1002=FACE_OUTER_BOUND('',#1418,.T.);
#1003=FACE_OUTER_BOUND('',#1419,.T.);
#1403=EDGE_LOOP('',(#4513,#4514,#4515,#4516));
#1404=EDGE_LOOP('',(#4517,#4518,#4519,#4520));
#1405=EDGE_LOOP('',(#4521,#4522,#4523,#4524));
#1406=EDGE_LOOP('',(#4525,#4526,#4527,#4528));
#1407=EDGE_LOOP('',(#4529,#4530,#4531,#4532));
#1408=EDGE_LOOP('',(#4533,#4534,#4535,#4536));
#1409=EDGE_LOOP('',(#4537,#4538,#4539,#4540,#4541,#4542));
#1410=EDGE_LOOP('',(#4543,#4544,#4545,#4546,#4547,#4548));
#1411=EDGE_LOOP('',(#4549));
#1412=EDGE_LOOP('',(#4550));
#1413=EDGE_LOOP('',(#4551,#4552,#4553,#4554));
#1414=EDGE_LOOP('',(#4555,#4556,#4557,#4558));
#1415=EDGE_LOOP('',(#4559,#4560,#4561,#4562));
#1416=EDGE_LOOP('',(#4563));
#1417=EDGE_LOOP('',(#4564));
#1418=EDGE_LOOP('',(#4565,#4566,#4567,#4568));
#1419=EDGE_LOOP('',(#4569,#4570,#4571,#4572));
#1755=LINE('',#9633,#2065);
#1756=LINE('',#9635,#2066);
#1757=LINE('',#9637,#2067);
#1758=LINE('',#9638,#2068);
#1759=LINE('',#9641,#2069);
#1760=LINE('',#9643,#2070);
#1761=LINE('',#9644,#2071);
#1762=LINE('',#9647,#2072);
#1763=LINE('',#9649,#2073);
#1764=LINE('',#9650,#2074);
#1765=LINE('',#9653,#2075);
#1766=LINE('',#9655,#2076);
#1767=LINE('',#9656,#2077);
#1768=LINE('',#9659,#2078);
#1769=LINE('',#9661,#2079);
#1770=LINE('',#9662,#2080);
#1771=LINE('',#9664,#2081);
#1772=LINE('',#9665,#2082);
#1773=LINE('',#9677,#2083);
#1774=LINE('',#9681,#2084);
#1775=LINE('',#9685,#2085);
#1776=LINE('',#9692,#2086);
#1777=LINE('',#9694,#2087);
#2065=VECTOR('',#7607,1.);
#2066=VECTOR('',#7608,1.);
#2067=VECTOR('',#7609,1.);
#2068=VECTOR('',#7610,1.);
#2069=VECTOR('',#7613,1.);
#2070=VECTOR('',#7614,1.);
#2071=VECTOR('',#7615,1.);
#2072=VECTOR('',#7618,1.);
#2073=VECTOR('',#7619,1.);
#2074=VECTOR('',#7620,1.);
#2075=VECTOR('',#7623,1.);
#2076=VECTOR('',#7624,1.);
#2077=VECTOR('',#7625,1.);
#2078=VECTOR('',#7628,1.);
#2079=VECTOR('',#7629,1.);
#2080=VECTOR('',#7630,1.);
#2081=VECTOR('',#7633,1.);
#2082=VECTOR('',#7634,1.);
#2083=VECTOR('',#7651,0.325);
#2084=VECTOR('',#7656,0.35);
#2085=VECTOR('',#7661,0.335);
#2086=VECTOR('',#7670,0.21);
#2087=VECTOR('',#7673,0.2);
#2347=CIRCLE('',#6178,0.1954);
#2348=CIRCLE('',#6180,0.3);
#2349=CIRCLE('',#6182,0.35);
#2350=CIRCLE('',#6184,0.35);
#2351=CIRCLE('',#6186,0.32);
#2352=CIRCLE('',#6188,0.22);
#2353=CIRCLE('',#6190,0.1954);
#2767=VERTEX_POINT('',#9631);
#2768=VERTEX_POINT('',#9632);
#2769=VERTEX_POINT('',#9634);
#2770=VERTEX_POINT('',#9636);
#2771=VERTEX_POINT('',#9640);
#2772=VERTEX_POINT('',#9642);
#2773=VERTEX_POINT('',#9646);
#2774=VERTEX_POINT('',#9648);
#2775=VERTEX_POINT('',#9652);
#2776=VERTEX_POINT('',#9654);
#2777=VERTEX_POINT('',#9658);
#2778=VERTEX_POINT('',#9660);
#2779=VERTEX_POINT('',#9669);
#2780=VERTEX_POINT('',#9672);
#2781=VERTEX_POINT('',#9675);
#2782=VERTEX_POINT('',#9679);
#2783=VERTEX_POINT('',#9683);
#2784=VERTEX_POINT('',#9687);
#2785=VERTEX_POINT('',#9690);
#3374=EDGE_CURVE('',#2767,#2768,#1755,.T.);
#3375=EDGE_CURVE('',#2768,#2769,#1756,.T.);
#3376=EDGE_CURVE('',#2769,#2770,#1757,.T.);
#3377=EDGE_CURVE('',#2767,#2770,#1758,.T.);
#3378=EDGE_CURVE('',#2768,#2771,#1759,.T.);
#3379=EDGE_CURVE('',#2771,#2772,#1760,.T.);
#3380=EDGE_CURVE('',#2772,#2769,#1761,.T.);
#3381=EDGE_CURVE('',#2771,#2773,#1762,.T.);
#3382=EDGE_CURVE('',#2773,#2774,#1763,.T.);
#3383=EDGE_CURVE('',#2774,#2772,#1764,.T.);
#3384=EDGE_CURVE('',#2773,#2775,#1765,.T.);
#3385=EDGE_CURVE('',#2775,#2776,#1766,.T.);
#3386=EDGE_CURVE('',#2776,#2774,#1767,.T.);
#3387=EDGE_CURVE('',#2775,#2777,#1768,.T.);
#3388=EDGE_CURVE('',#2777,#2778,#1769,.T.);
#3389=EDGE_CURVE('',#2778,#2776,#1770,.T.);
#3390=EDGE_CURVE('',#2777,#2767,#1771,.T.);
#3391=EDGE_CURVE('',#2770,#2778,#1772,.T.);
#3392=EDGE_CURVE('',#2779,#2779,#2347,.T.);
#3393=EDGE_CURVE('',#2780,#2780,#2348,.T.);
#3394=EDGE_CURVE('',#2781,#2781,#2349,.T.);
#3395=EDGE_CURVE('',#2781,#2780,#1773,.T.);
#3396=EDGE_CURVE('',#2782,#2782,#2350,.T.);
#3397=EDGE_CURVE('',#2782,#2781,#1774,.T.);
#3398=EDGE_CURVE('',#2783,#2783,#2351,.T.);
#3399=EDGE_CURVE('',#2783,#2782,#1775,.T.);
#3400=EDGE_CURVE('',#2784,#2784,#2352,.T.);
#3401=EDGE_CURVE('',#2785,#2785,#2353,.F.);
#3402=EDGE_CURVE('',#2785,#2784,#1776,.T.);
#3403=EDGE_CURVE('',#2779,#2785,#1777,.T.);
#4513=ORIENTED_EDGE('',*,*,#3374,.T.);
#4514=ORIENTED_EDGE('',*,*,#3375,.T.);
#4515=ORIENTED_EDGE('',*,*,#3376,.T.);
#4516=ORIENTED_EDGE('',*,*,#3377,.F.);
#4517=ORIENTED_EDGE('',*,*,#3378,.T.);
#4518=ORIENTED_EDGE('',*,*,#3379,.T.);
#4519=ORIENTED_EDGE('',*,*,#3380,.T.);
#4520=ORIENTED_EDGE('',*,*,#3375,.F.);
#4521=ORIENTED_EDGE('',*,*,#3381,.T.);
#4522=ORIENTED_EDGE('',*,*,#3382,.T.);
#4523=ORIENTED_EDGE('',*,*,#3383,.T.);
#4524=ORIENTED_EDGE('',*,*,#3379,.F.);
#4525=ORIENTED_EDGE('',*,*,#3384,.T.);
#4526=ORIENTED_EDGE('',*,*,#3385,.T.);
#4527=ORIENTED_EDGE('',*,*,#3386,.T.);
#4528=ORIENTED_EDGE('',*,*,#3382,.F.);
#4529=ORIENTED_EDGE('',*,*,#3387,.T.);
#4530=ORIENTED_EDGE('',*,*,#3388,.T.);
#4531=ORIENTED_EDGE('',*,*,#3389,.T.);
#4532=ORIENTED_EDGE('',*,*,#3385,.F.);
#4533=ORIENTED_EDGE('',*,*,#3390,.T.);
#4534=ORIENTED_EDGE('',*,*,#3377,.T.);
#4535=ORIENTED_EDGE('',*,*,#3391,.T.);
#4536=ORIENTED_EDGE('',*,*,#3388,.F.);
#4537=ORIENTED_EDGE('',*,*,#3390,.F.);
#4538=ORIENTED_EDGE('',*,*,#3387,.F.);
#4539=ORIENTED_EDGE('',*,*,#3384,.F.);
#4540=ORIENTED_EDGE('',*,*,#3381,.F.);
#4541=ORIENTED_EDGE('',*,*,#3378,.F.);
#4542=ORIENTED_EDGE('',*,*,#3374,.F.);
#4543=ORIENTED_EDGE('',*,*,#3391,.F.);
#4544=ORIENTED_EDGE('',*,*,#3376,.F.);
#4545=ORIENTED_EDGE('',*,*,#3380,.F.);
#4546=ORIENTED_EDGE('',*,*,#3383,.F.);
#4547=ORIENTED_EDGE('',*,*,#3386,.F.);
#4548=ORIENTED_EDGE('',*,*,#3389,.F.);
#4549=ORIENTED_EDGE('',*,*,#3392,.F.);
#4550=ORIENTED_EDGE('',*,*,#3393,.F.);
#4551=ORIENTED_EDGE('',*,*,#3394,.F.);
#4552=ORIENTED_EDGE('',*,*,#3395,.T.);
#4553=ORIENTED_EDGE('',*,*,#3393,.T.);
#4554=ORIENTED_EDGE('',*,*,#3395,.F.);
#4555=ORIENTED_EDGE('',*,*,#3396,.F.);
#4556=ORIENTED_EDGE('',*,*,#3397,.T.);
#4557=ORIENTED_EDGE('',*,*,#3394,.T.);
#4558=ORIENTED_EDGE('',*,*,#3397,.F.);
#4559=ORIENTED_EDGE('',*,*,#3398,.F.);
#4560=ORIENTED_EDGE('',*,*,#3399,.T.);
#4561=ORIENTED_EDGE('',*,*,#3396,.T.);
#4562=ORIENTED_EDGE('',*,*,#3399,.F.);
#4563=ORIENTED_EDGE('',*,*,#3398,.T.);
#4564=ORIENTED_EDGE('',*,*,#3400,.F.);
#4565=ORIENTED_EDGE('',*,*,#3401,.F.);
#4566=ORIENTED_EDGE('',*,*,#3402,.T.);
#4567=ORIENTED_EDGE('',*,*,#3400,.T.);
#4568=ORIENTED_EDGE('',*,*,#3402,.F.);
#4569=ORIENTED_EDGE('',*,*,#3392,.T.);
#4570=ORIENTED_EDGE('',*,*,#3403,.T.);
#4571=ORIENTED_EDGE('',*,*,#3401,.T.);
#4572=ORIENTED_EDGE('',*,*,#3403,.F.);
#4954=CYLINDRICAL_SURFACE('',#6183,0.35);
#4955=CYLINDRICAL_SURFACE('',#6191,0.1954);
#5200=ADVANCED_FACE('',(#988),#719,.F.);
#5201=ADVANCED_FACE('',(#989),#720,.F.);
#5202=ADVANCED_FACE('',(#990),#721,.F.);
#5203=ADVANCED_FACE('',(#991),#722,.F.);
#5204=ADVANCED_FACE('',(#992),#723,.F.);
#5205=ADVANCED_FACE('',(#993),#724,.F.);
#5206=ADVANCED_FACE('',(#994),#725,.F.);
#5207=ADVANCED_FACE('',(#995),#726,.F.);
#5208=ADVANCED_FACE('',(#996),#727,.F.);
#5209=ADVANCED_FACE('',(#997),#728,.T.);
#5210=ADVANCED_FACE('',(#998),#314,.T.);
#5211=ADVANCED_FACE('',(#999),#4954,.T.);
#5212=ADVANCED_FACE('',(#1000),#315,.T.);
#5213=ADVANCED_FACE('',(#1001,#582),#729,.T.);
#5214=ADVANCED_FACE('',(#1002),#316,.T.);
#5215=ADVANCED_FACE('',(#1003),#4955,.T.);
#5325=CLOSED_SHELL('',(#5200,#5201,#5202,#5203,#5204,#5205,#5206,#5207));
#5326=CLOSED_SHELL('',(#5208,#5209,#5210,#5211,#5212,#5213,#5214,#5215));
#6168=AXIS2_PLACEMENT_3D('',#9629,#7603,#7604);
#6169=AXIS2_PLACEMENT_3D('',#9630,#7605,#7606);
#6170=AXIS2_PLACEMENT_3D('',#9639,#7611,#7612);
#6171=AXIS2_PLACEMENT_3D('',#9645,#7616,#7617);
#6172=AXIS2_PLACEMENT_3D('',#9651,#7621,#7622);
#6173=AXIS2_PLACEMENT_3D('',#9657,#7626,#7627);
#6174=AXIS2_PLACEMENT_3D('',#9663,#7631,#7632);
#6175=AXIS2_PLACEMENT_3D('',#9666,#7635,#7636);
#6176=AXIS2_PLACEMENT_3D('',#9667,#7637,#7638);
#6177=AXIS2_PLACEMENT_3D('',#9668,#7639,#7640);
#6178=AXIS2_PLACEMENT_3D('',#9670,#7641,#7642);
#6179=AXIS2_PLACEMENT_3D('',#9671,#7643,#7644);
#6180=AXIS2_PLACEMENT_3D('',#9673,#7645,#7646);
#6181=AXIS2_PLACEMENT_3D('',#9674,#7647,#7648);
#6182=AXIS2_PLACEMENT_3D('',#9676,#7649,#7650);
#6183=AXIS2_PLACEMENT_3D('',#9678,#7652,#7653);
#6184=AXIS2_PLACEMENT_3D('',#9680,#7654,#7655);
#6185=AXIS2_PLACEMENT_3D('',#9682,#7657,#7658);
#6186=AXIS2_PLACEMENT_3D('',#9684,#7659,#7660);
#6187=AXIS2_PLACEMENT_3D('',#9686,#7662,#7663);
#6188=AXIS2_PLACEMENT_3D('',#9688,#7664,#7665);
#6189=AXIS2_PLACEMENT_3D('',#9689,#7666,#7667);
#6190=AXIS2_PLACEMENT_3D('',#9691,#7668,#7669);
#6191=AXIS2_PLACEMENT_3D('',#9693,#7671,#7672);
#7603=DIRECTION('axis',(0.,0.,1.));
#7604=DIRECTION('refdir',(1.,0.,0.));
#7605=DIRECTION('center_axis',(0.866025403784439,0.,-0.5));
#7606=DIRECTION('ref_axis',(0.5,0.,0.866025403784439));
#7607=DIRECTION('',(-0.5,0.,-0.866025403784439));
#7608=DIRECTION('',(0.,-1.,0.));
#7609=DIRECTION('',(0.5,0.,0.866025403784439));
#7610=DIRECTION('',(0.,-1.,0.));
#7611=DIRECTION('center_axis',(1.60246890531964E-16,0.,-1.));
#7612=DIRECTION('ref_axis',(1.,0.,1.60246890531964E-16));
#7613=DIRECTION('',(-1.,0.,-1.60246890531964E-16));
#7614=DIRECTION('',(0.,-1.,0.));
#7615=DIRECTION('',(1.,0.,1.60246890531964E-16));
#7616=DIRECTION('center_axis',(-0.866025403784439,0.,-0.5));
#7617=DIRECTION('ref_axis',(0.5,0.,-0.866025403784439));
#7618=DIRECTION('',(-0.5,0.,0.866025403784439));
#7619=DIRECTION('',(0.,-1.,0.));
#7620=DIRECTION('',(0.5,0.,-0.866025403784439));
#7621=DIRECTION('center_axis',(-0.866025403784439,0.,0.5));
#7622=DIRECTION('ref_axis',(-0.5,0.,-0.866025403784439));
#7623=DIRECTION('',(0.5,0.,0.866025403784439));
#7624=DIRECTION('',(0.,-1.,0.));
#7625=DIRECTION('',(-0.5,0.,-0.866025403784439));
#7626=DIRECTION('center_axis',(-1.60246890531964E-16,0.,1.));
#7627=DIRECTION('ref_axis',(-1.,0.,-1.60246890531964E-16));
#7628=DIRECTION('',(1.,0.,1.60246890531964E-16));
#7629=DIRECTION('',(0.,-1.,0.));
#7630=DIRECTION('',(-1.,0.,-1.60246890531964E-16));
#7631=DIRECTION('center_axis',(0.866025403784439,0.,0.5));
#7632=DIRECTION('ref_axis',(-0.5,0.,0.866025403784439));
#7633=DIRECTION('',(0.5,0.,-0.866025403784439));
#7634=DIRECTION('',(-0.5,0.,0.866025403784439));
#7635=DIRECTION('center_axis',(0.,1.,0.));
#7636=DIRECTION('ref_axis',(1.,0.,0.));
#7637=DIRECTION('center_axis',(0.,-1.,0.));
#7638=DIRECTION('ref_axis',(0.,0.,-1.));
#7639=DIRECTION('center_axis',(0.,1.,0.));
#7640=DIRECTION('ref_axis',(1.,0.,0.));
#7641=DIRECTION('center_axis',(0.,1.,0.));
#7642=DIRECTION('ref_axis',(1.,0.,0.));
#7643=DIRECTION('center_axis',(0.,1.,0.));
#7644=DIRECTION('ref_axis',(0.,0.,1.));
#7645=DIRECTION('center_axis',(0.,-1.,0.));
#7646=DIRECTION('ref_axis',(1.,0.,0.));
#7647=DIRECTION('center_axis',(0.,-1.,0.));
#7648=DIRECTION('ref_axis',(1.,0.,0.));
#7649=DIRECTION('center_axis',(0.,-1.,0.));
#7650=DIRECTION('ref_axis',(1.,0.,0.));
#7651=DIRECTION('',(0.707106781186547,0.707106781186548,8.65956056235493E-17));
#7652=DIRECTION('center_axis',(0.,-1.,0.));
#7653=DIRECTION('ref_axis',(1.,0.,0.));
#7654=DIRECTION('center_axis',(0.,-1.,0.));
#7655=DIRECTION('ref_axis',(1.,0.,0.));
#7656=DIRECTION('',(0.,1.,0.));
#7657=DIRECTION('center_axis',(0.,1.,0.));
#7658=DIRECTION('ref_axis',(1.,0.,0.));
#7659=DIRECTION('center_axis',(0.,-1.,0.));
#7660=DIRECTION('ref_axis',(1.,0.,0.));
#7661=DIRECTION('',(-0.707106781186547,0.707106781186548,-8.65956056235493E-17));
#7662=DIRECTION('center_axis',(0.,-1.,0.));
#7663=DIRECTION('ref_axis',(0.,0.,-1.));
#7664=DIRECTION('center_axis',(0.,-1.,0.));
#7665=DIRECTION('ref_axis',(1.,0.,0.));
#7666=DIRECTION('center_axis',(0.,1.,0.));
#7667=DIRECTION('ref_axis',(1.,0.,0.));
#7668=DIRECTION('center_axis',(0.,1.,0.));
#7669=DIRECTION('ref_axis',(1.,0.,0.));
#7670=DIRECTION('',(-0.447213595499958,0.894427190999916,-5.47678698264203E-17));
#7671=DIRECTION('center_axis',(0.,-1.,0.));
#7672=DIRECTION('ref_axis',(1.,0.,0.));
#7673=DIRECTION('',(0.,1.,0.));
#9629=CARTESIAN_POINT('',(0.,0.,0.));
#9630=CARTESIAN_POINT('Origin',(0.0866025403784439,-0.4,-0.15));
#9631=CARTESIAN_POINT('',(0.173205080756888,-0.4,0.));
#9632=CARTESIAN_POINT('',(0.0866025403784439,-0.4,-0.15));
#9633=CARTESIAN_POINT('',(0.173205080756888,-0.4,0.));
#9634=CARTESIAN_POINT('',(0.0866025403784439,-0.64,-0.15));
#9635=CARTESIAN_POINT('',(0.0866025403784439,-0.4,-0.15));
#9636=CARTESIAN_POINT('',(0.173205080756888,-0.64,0.));
#9637=CARTESIAN_POINT('',(0.173205080756888,-0.64,0.));
#9638=CARTESIAN_POINT('',(0.173205080756888,-0.4,0.));
#9639=CARTESIAN_POINT('Origin',(-0.0866025403784438,-0.4,-0.15));
#9640=CARTESIAN_POINT('',(-0.0866025403784438,-0.4,-0.15));
#9641=CARTESIAN_POINT('',(0.0866025403784439,-0.4,-0.15));
#9642=CARTESIAN_POINT('',(-0.0866025403784438,-0.64,-0.15));
#9643=CARTESIAN_POINT('',(-0.0866025403784438,-0.4,-0.15));
#9644=CARTESIAN_POINT('',(0.0866025403784439,-0.64,-0.15));
#9645=CARTESIAN_POINT('Origin',(-0.173205080756888,-0.4,-2.77555756156289E-17));
#9646=CARTESIAN_POINT('',(-0.173205080756888,-0.4,-2.12115047744981E-17));
#9647=CARTESIAN_POINT('',(-0.0866025403784438,-0.4,-0.15));
#9648=CARTESIAN_POINT('',(-0.173205080756888,-0.64,-2.77555756156289E-17));
#9649=CARTESIAN_POINT('',(-0.173205080756888,-0.4,-2.12115047744981E-17));
#9650=CARTESIAN_POINT('',(-0.0866025403784438,-0.64,-0.15));
#9651=CARTESIAN_POINT('Origin',(-0.0866025403784439,-0.4,0.15));
#9652=CARTESIAN_POINT('',(-0.0866025403784439,-0.4,0.15));
#9653=CARTESIAN_POINT('',(-0.173205080756888,-0.4,-2.12115047744981E-17));
#9654=CARTESIAN_POINT('',(-0.0866025403784439,-0.64,0.15));
#9655=CARTESIAN_POINT('',(-0.0866025403784439,-0.4,0.15));
#9656=CARTESIAN_POINT('',(-0.173205080756888,-0.64,-2.12115047744981E-17));
#9657=CARTESIAN_POINT('Origin',(0.0866025403784439,-0.4,0.15));
#9658=CARTESIAN_POINT('',(0.0866025403784439,-0.4,0.15));
#9659=CARTESIAN_POINT('',(-0.0866025403784439,-0.4,0.15));
#9660=CARTESIAN_POINT('',(0.0866025403784439,-0.64,0.15));
#9661=CARTESIAN_POINT('',(0.0866025403784439,-0.4,0.15));
#9662=CARTESIAN_POINT('',(-0.0866025403784439,-0.64,0.15));
#9663=CARTESIAN_POINT('Origin',(0.173205080756888,-0.4,0.));
#9664=CARTESIAN_POINT('',(0.0866025403784439,-0.4,0.15));
#9665=CARTESIAN_POINT('',(0.0866025403784439,-0.64,0.15));
#9666=CARTESIAN_POINT('Origin',(0.,-0.4,-2.77555756156289E-17));
#9667=CARTESIAN_POINT('Origin',(0.,-0.64,-2.77555756156289E-17));
#9668=CARTESIAN_POINT('Origin',(0.,-1.,0.));
#9669=CARTESIAN_POINT('',(-0.1954,-1.,2.39295984553393E-17));
#9670=CARTESIAN_POINT('Origin',(0.,-1.,0.));
#9671=CARTESIAN_POINT('Origin',(0.3,0.4,0.));
#9672=CARTESIAN_POINT('',(-0.3,0.4,-3.67394039744206E-17));
#9673=CARTESIAN_POINT('Origin',(0.,0.4,0.));
#9674=CARTESIAN_POINT('Origin',(0.,0.375,0.));
#9675=CARTESIAN_POINT('',(-0.35,0.35,-4.28626379701573E-17));
#9676=CARTESIAN_POINT('Origin',(0.,0.35,0.));
#9677=CARTESIAN_POINT('',(-0.325,0.375,-3.9801020972289E-17));
#9678=CARTESIAN_POINT('Origin',(0.,0.19,0.));
#9679=CARTESIAN_POINT('',(-0.35,0.03,-4.28626379701574E-17));
#9680=CARTESIAN_POINT('Origin',(0.,0.03,0.));
#9681=CARTESIAN_POINT('',(-0.35,0.19,-4.28626379701574E-17));
#9682=CARTESIAN_POINT('Origin',(0.,0.0149999999999999,0.));
#9683=CARTESIAN_POINT('',(-0.32,-3.29597460435593E-17,-3.91886975727153E-17));
#9684=CARTESIAN_POINT('Origin',(0.,0.,0.));
#9685=CARTESIAN_POINT('',(-0.335,0.0149999999999999,-4.10256677714363E-17));
#9686=CARTESIAN_POINT('Origin',(0.22,0.,0.));
#9687=CARTESIAN_POINT('',(-0.22,-6.93889390390723E-18,-2.69422295812418E-17));
#9688=CARTESIAN_POINT('Origin',(0.,0.,0.));
#9689=CARTESIAN_POINT('Origin',(0.,-0.02,0.));
#9690=CARTESIAN_POINT('',(-0.1954,-0.0492,2.39295984553393E-17));
#9691=CARTESIAN_POINT('Origin',(0.,-0.0492,0.));
#9692=CARTESIAN_POINT('',(-0.21,-0.02,-2.57175827820944E-17));
#9693=CARTESIAN_POINT('Origin',(0.,-0.8,0.));
#9694=CARTESIAN_POINT('',(-0.1954,-0.8,-2.39295984553393E-17));
#10460=UNCERTAINTY_MEASURE_WITH_UNIT(LENGTH_MEASURE(0.001),#10511,
'DISTANCE_ACCURACY_VALUE',
'Maximum model space distance between geometric entities at asserted c
onnectivities');
#10471=UNCERTAINTY_MEASURE_WITH_UNIT(LENGTH_MEASURE(0.001),#10511,
'DISTANCE_ACCURACY_VALUE',
'Maximum model space distance between geometric entities at asserted c
onnectivities');
#10499=(
GEOMETRIC_REPRESENTATION_CONTEXT(3)
GLOBAL_UNCERTAINTY_ASSIGNED_CONTEXT((#10460))
GLOBAL_UNIT_ASSIGNED_CONTEXT((#10511,#10513,#10514))
REPRESENTATION_CONTEXT('','3D')
);
#10510=(
GEOMETRIC_REPRESENTATION_CONTEXT(3)
GLOBAL_UNCERTAINTY_ASSIGNED_CONTEXT((#10471))
GLOBAL_UNIT_ASSIGNED_CONTEXT((#10511,#10513,#10514))
REPRESENTATION_CONTEXT('','3D')
);
#10511=(
LENGTH_UNIT()
NAMED_UNIT(*)
SI_UNIT(.CENTI.,.METRE.)
);
#10513=(
NAMED_UNIT(*)
PLANE_ANGLE_UNIT()
SI_UNIT($,.RADIAN.)
);
#10514=(
NAMED_UNIT(*)
SI_UNIT($,.STERADIAN.)
SOLID_ANGLE_UNIT()
);
#10542=SHAPE_DEFINITION_REPRESENTATION(#10585,#10672);
#10585=PRODUCT_DEFINITION_SHAPE('',$,#10711);
#10672=SHAPE_REPRESENTATION('',(#6168),#10499);
#10683=PRODUCT_DEFINITION_CONTEXT('part definition',#10799,'design');
#10711=PRODUCT_DEFINITION('M4x10 handle screw','M4x10 handle screw',#10749,
#10683);
#10749=PRODUCT_DEFINITION_FORMATION('',$,#10828);
#10799=APPLICATION_CONTEXT(
'Core Data for Automotive Mechanical Design Process');
#10800=PRODUCT_CONTEXT('part definition',#10799,'mechanical');
#10828=PRODUCT('M4x10 handle screw','M4x10 handle screw',
'M4x10 handle screw',(#10800));
#10909=COLOUR_RGB('Black',0.12,0.14,0.17);
#10910=FILL_AREA_STYLE_COLOUR('',#10909);
#10911=FILL_AREA_STYLE('',(#10910));
#10912=SURFACE_STYLE_FILL_AREA(#10911);
#10913=SURFACE_SIDE_STYLE('',(#10912));
#10914=SURFACE_STYLE_USAGE(.BOTH.,#10913);
#10915=PRESENTATION_STYLE_ASSIGNMENT((#10914));
ENDSEC;
END-ISO-10303-21;
